ISO-10303-21;
HEADER;
FILE_DESCRIPTION (('STEP AP214'),
    '1' );
FILE_NAME ('hex bolt gradec_iso_ISO 4016 - M12 x 55 x 30-WN.step',
    '2026-10-08T00:39:10',
    ( '' ),
    ( '' ),
    'SwSTEP 2.0',
    'SolidWorks 2025',
    '' );
FILE_SCHEMA (( 'AUTOMOTIVE_DESIGN' ));
ENDSEC;

DATA;
#41=PLANE ( 'NONE',  #1345 ) ;
#85=CARTESIAN_POINT ( 'NONE',  ( 7.350000000000001421, 0.000000000000000000, 0.000000000000000000 ) ) ;
#121=EDGE_CURVE ( 'NONE', #7971, #3301, #6530, .T. ) ;
#149=EDGE_CURVE ( 'NONE', #12149, #16123, #12294, .T. ) ;
#150=ORIENTED_EDGE ( 'NONE', *, *, #14501, .F. ) ;
#153=DIRECTION ( 'NONE',  ( 0.000000000000000000, 0.000000000000000000, -1.000000000000000000 ) ) ;
#166=VERTEX_POINT ( 'NONE', #19011 ) ;
#204=DIRECTION ( 'NONE',  ( -1.000000000000000000, -0.000000000000000000, -0.000000000000000000 ) ) ;
#275=DIRECTION ( 'NONE',  ( 1.000000000000000000, 0.000000000000000000, -0.000000000000000000 ) ) ;
#281=ORIENTED_EDGE ( 'NONE', *, *, #5638, .F. ) ;
#300=LINE ( 'NONE', #15954, #4521 ) ;
#323=SHAPE_DEFINITION_REPRESENTATION ( #15864, #15821 ) ;
#349=CARTESIAN_POINT ( 'NONE',  ( 0.000000000000000000, -7.794228634059948035, -4.499999999999999112 ) ) ;
#352=ORIENTED_EDGE ( 'NONE', *, *, #1999, .T. ) ;
#448=FACE_OUTER_BOUND ( 'NONE', #5295, .T. ) ;
#491=DIRECTION ( 'NONE',  ( -1.000000000000000000, -0.000000000000000000, -0.000000000000000000 ) ) ;
#502=ORIENTED_EDGE ( 'NONE', *, *, #7085, .F. ) ;
#517=CARTESIAN_POINT ( 'NONE',  ( 7.350000000000001421, 0.000000000000000000, 0.000000000000000000 ) ) ;
#555=EDGE_CURVE ( 'NONE', #13410, #10176, #5141, .T. ) ;
#556=ORIENTED_EDGE ( 'NONE', *, *, #14355, .F. ) ;
#593=CARTESIAN_POINT ( 'NONE',  ( 0.07568653364412687712, -1.751902528157470718, -8.999999999999998224 ) ) ;
#656=EDGE_CURVE ( 'NONE', #12589, #3734, #6149, .T. ) ;
#670=VECTOR ( 'NONE', #2856, 1000.000000000000114 ) ;
#682=AXIS2_PLACEMENT_3D ( 'NONE', #5183, #17564, #3537 ) ;
#699=FACE_OUTER_BOUND ( 'NONE', #9006, .T. ) ;
#702=CARTESIAN_POINT ( 'NONE',  ( 7.950000000000000178, 0.000000000000000000, 0.000000000000000000 ) ) ;
#742=CARTESIAN_POINT ( 'NONE',  ( 7.350000000000000533, 5.196152422706624030, -9.000000000000001776 ) ) ;
#746=AXIS2_PLACEMENT_3D ( 'NONE', #2840, #16555, #12127 ) ;
#869=CARTESIAN_POINT ( 'NONE',  ( 62.95000000000000284, 0.000000000000000000, 5.035999999999999588 ) ) ;
#875=ORIENTED_EDGE ( 'NONE', *, *, #149, .F. ) ;
#885=LINE ( 'NONE', #16552, #16463 ) ;
#907=ORIENTED_EDGE ( 'NONE', *, *, #964, .T. ) ;
#964=EDGE_CURVE ( 'NONE', #10176, #13410, #4043, .T. ) ;
#976=CARTESIAN_POINT ( 'NONE',  ( 0.5584673446549194287, 9.967293815311103700, -0.7361406979141406071 ) ) ;
#1030=ORIENTED_EDGE ( 'NONE', *, *, #1534, .T. ) ;
#1046=FACE_OUTER_BOUND ( 'NONE', #12800, .T. ) ;
#1102=AXIS2_PLACEMENT_3D ( 'NONE', #13954, #20197, #153 ) ;
#1160=PLANE ( 'NONE',  #3024 ) ;
#1177=AXIS2_PLACEMENT_3D ( 'NONE', #18806, #275, #4789 ) ;
#1184=ORIENTED_EDGE ( 'NONE', *, *, #5153, .T. ) ;
#1232=CARTESIAN_POINT ( 'NONE',  ( 0.000000000000000000, -3.004629197474327134E-15, 9.000000000000000000 ) ) ;
#1278=CONICAL_SURFACE ( 'NONE', #8779, 9.000000000000000000, 1.047197551196600296 ) ;
#1345=AXIS2_PLACEMENT_3D ( 'NONE', #10974, #13736, #19980 ) ;
#1376=ADVANCED_FACE ( 'NONE', ( #7608 ), #8843, .F. ) ;
#1391=CARTESIAN_POINT ( 'NONE',  ( 0.5612050131688013366, 4.355613924421562366, 9.000000000000003553 ) ) ;
#1431=ORIENTED_EDGE ( 'NONE', *, *, #13655, .F. ) ;
#1480=ADVANCED_FACE ( 'NONE', ( #4143 ), #7310, .F. ) ;
#1504=ORIENTED_EDGE ( 'NONE', *, *, #5179, .T. ) ;
#1514=CARTESIAN_POINT ( 'NONE',  ( 0.000000000000000000, 7.794228634059941818, 4.500000000000007994 ) ) ;
#1534=EDGE_CURVE ( 'NONE', #4193, #12149, #3718, .T. ) ;
#1542=ADVANCED_FACE ( 'NONE', ( #15808 ), #19086, .T. ) ;
#1612=AXIS2_PLACEMENT_3D ( 'NONE', #19576, #2494, #2400 ) ;
#1614=CARTESIAN_POINT ( 'NONE',  ( 7.950000000000000178, -10.39230484541326582, 0.000000000000000000 ) ) ;
#1657=EDGE_LOOP ( 'NONE', ( #11287, #15226, #11669 ) ) ;
#1688=EDGE_LOOP ( 'NONE', ( #7188, #16034, #5863 ) ) ;
#1784=AXIS2_PLACEMENT_3D ( 'NONE', #15184, #13748, #19894 ) ;
#1796=LINE ( 'NONE', #12732, #8766 ) ;
#1820=ORIENTED_EDGE ( 'NONE', *, *, #18588, .T. ) ;
#1863=ORIENTED_EDGE ( 'NONE', *, *, #18363, .F. ) ;
#1957=ORIENTED_EDGE ( 'NONE', *, *, #6019, .T. ) ;
#1975=FILL_AREA_STYLE_COLOUR ( '', #18077 ) ;
#1990=EDGE_CURVE ( 'NONE', #13146, #5943, #11144, .T. ) ;
#1999=EDGE_CURVE ( 'NONE', #2094, #6828, #14327, .T. ) ;
#2021=PRODUCT_DEFINITION_FORMATION_WITH_SPECIFIED_SOURCE ( 'ANY', '', #18804, .NOT_KNOWN. ) ;
#2078=ORIENTED_EDGE ( 'NONE', *, *, #9346, .T. ) ;
#2080=DIRECTION ( 'NONE',  ( -1.000000000000000000, -0.000000000000000000, -0.000000000000000000 ) ) ;
#2094=VERTEX_POINT ( 'NONE', #13705 ) ;
#2136=FACE_OUTER_BOUND ( 'NONE', #8142, .T. ) ;
#2146=DIRECTION ( 'NONE',  ( 1.000000000000000000, 0.000000000000000000, 0.000000000000000000 ) ) ;
#2147=CONICAL_SURFACE ( 'NONE', #3034, 9.000000000000000000, 1.047197551196600296 ) ;
#2151=CARTESIAN_POINT ( 'NONE',  ( 0.3570196857253480904, -9.540868182094900618, -1.474731560294321175 ) ) ;
#2185=VECTOR ( 'NONE', #2596, 1000.000000000000000 ) ;
#2198=AXIS2_PLACEMENT_3D ( 'NONE', #7177, #8698, #10324 ) ;
#2204=CARTESIAN_POINT ( 'NONE',  ( 0.8038475772933615371, 5.196152422706624030, -9.000000000000001776 ) ) ;
#2294=LINE ( 'NONE', #742, #4007 ) ;
#2360=ORIENTED_EDGE ( 'NONE', *, *, #5173, .F. ) ;
#2387=( NAMED_UNIT ( * ) PLANE_ANGLE_UNIT ( ) SI_UNIT ( $, .RADIAN. ) );
#2400=DIRECTION ( 'NONE',  ( 0.000000000000000000, 0.000000000000000000, 1.000000000000000000 ) ) ;
#2402=EDGE_CURVE ( 'NONE', #9431, #10259, #19626, .T. ) ;
#2438=FACE_OUTER_BOUND ( 'NONE', #6937, .T. ) ;
#2494=DIRECTION ( 'NONE',  ( -1.000000000000000000, -0.000000000000000000, -0.000000000000000000 ) ) ;
#2516=CARTESIAN_POINT ( 'NONE',  ( 0.8038475772933646457, -10.39230484541326582, 2.804506490479260738E-17 ) ) ;
#2533=VERTEX_POINT ( 'NONE', #14180 ) ;
#2577=LINE ( 'NONE', #13502, #11522 ) ;
#2596=DIRECTION ( 'NONE',  ( 0.000000000000000000, 1.000000000000000000, -3.338476886082577323E-16 ) ) ;
#2627=( GEOMETRIC_REPRESENTATION_CONTEXT ( 3 ) GLOBAL_UNCERTAINTY_ASSIGNED_CONTEXT ( ( #12345 ) ) GLOBAL_UNIT_ASSIGNED_CONTEXT ( ( #19961, #2387, #6276 ) ) REPRESENTATION_CONTEXT ( 'NONE', 'WORKASPACE' ) );
#2649=EDGE_LOOP ( 'NONE', ( #12745, #3338, #150, #10624, #6173, #3093 ) ) ;
#2685=CIRCLE ( 'NONE', #14117, 6.000000000000001776 ) ;
#2719=DIRECTION ( 'NONE',  ( 0.000000000000000000, 0.000000000000000000, 1.000000000000000000 ) ) ;
#2803=EDGE_LOOP ( 'NONE', ( #18386, #6220, #1957 ) ) ;
#2840=CARTESIAN_POINT ( 'NONE',  ( 61.98599999999999000, 0.000000000000000000, 0.000000000000000000 ) ) ;
#2846=DIRECTION ( 'NONE',  ( 0.000000000000000000, 0.000000000000000000, 1.000000000000000000 ) ) ;
#2856=DIRECTION ( 'NONE',  ( 0.000000000000000000, 0.4999999999999998335, -0.8660254037844387076 ) ) ;
#2857=CARTESIAN_POINT ( 'NONE',  ( 0.000000000000000000, -3.004629197474319246E-15, -9.000000000000000000 ) ) ;
#2902=LINE ( 'NONE', #13521, #2185 ) ;
#2921=CARTESIAN_POINT ( 'NONE',  ( 62.95000000000000284, 0.000000000000000000, 0.000000000000000000 ) ) ;
#2926=ADVANCED_FACE ( 'NONE', ( #13632 ), #41, .F. ) ;
#2953=CARTESIAN_POINT ( 'NONE',  ( 0.5590800469813600460, 5.620102221249812402, -8.265697409064610923 ) ) ;
#2993=VECTOR ( 'NONE', #17405, 1000.000000000000000 ) ;
#2994=ORIENTED_EDGE ( 'NONE', *, *, #4392, .F. ) ;
#3001=CARTESIAN_POINT ( 'NONE',  ( 7.350000000000001421, 0.000000000000000000, 0.000000000000000000 ) ) ;
#3024=AXIS2_PLACEMENT_3D ( 'NONE', #7401, #5882, #12095 ) ;
#3032=CARTESIAN_POINT ( 'NONE',  ( -4.340196821731034937E-15, 8.236864015571827125, -3.733333029993801233 ) ) ;
#3034=AXIS2_PLACEMENT_3D ( 'NONE', #6695, #12916, #5164 ) ;
#3089=CARTESIAN_POINT ( 'NONE',  ( 7.950000000000000178, -5.196152422706607155, 8.999999999999998224 ) ) ;
#3093=ORIENTED_EDGE ( 'NONE', *, *, #4161, .F. ) ;
#3095=SHAPE_REPRESENTATION_RELATIONSHIP ( 'NONE' , 'NONE' ,  #15821, #17527 ) ;
#3140=CONICAL_SURFACE ( 'NONE', #8990, 9.000000000000000000, 1.047197551196600296 ) ;
#3151=CARTESIAN_POINT ( 'NONE',  ( 0.8038475772933556529, -5.196152422706607155, 8.999999999999998224 ) ) ;
#3157=CARTESIAN_POINT ( 'NONE',  ( 0.000000000000000000, -3.004629197474327134E-15, 9.000000000000000000 ) ) ;
#3206=VECTOR ( 'NONE', #4105, 1000.000000000000114 ) ;
#3235=B_SPLINE_CURVE_WITH_KNOTS ( 'NONE', 3,
 ( #12063, #18327, #7470, #20160, #19850, #1232 ),
 .UNSPECIFIED., .F., .F.,
 ( 4, 2, 4 ),
 ( 0.009719890944573138583, 0.01235036185894304236, 0.01498083277331294441 ),
 .UNSPECIFIED. ) ;
#3258=CARTESIAN_POINT ( 'NONE',  ( 0.07661102881317774504, 6.914460432017340175, 6.023803224821316249 ) ) ;
#3261=PLANE ( 'NONE',  #16872 ) ;
#3281=CARTESIAN_POINT ( 'NONE',  ( 0.5590800469813620444, -9.968355046870076563, -0.7343025909353907421 ) ) ;
#3294=ORIENTED_EDGE ( 'NONE', *, *, #121, .T. ) ;
#3301=VERTEX_POINT ( 'NONE', #4511 ) ;
#3338=ORIENTED_EDGE ( 'NONE', *, *, #18363, .T. ) ;
#3353=CARTESIAN_POINT ( 'NONE',  ( 0.3563104543936346236, 6.049278984716044860, 7.522341449313135975 ) ) ;
#3397=AXIS2_PLACEMENT_3D ( 'NONE', #17888, #3862, #10107 ) ;
#3403=CIRCLE ( 'NONE', #7613, 5.035999999999999588 ) ;
#3497=ORIENTED_EDGE ( 'NONE', *, *, #5179, .F. ) ;
#3503=FACE_OUTER_BOUND ( 'NONE', #7245, .T. ) ;
#3505=FACE_OUTER_BOUND ( 'NONE', #15361, .T. ) ;
#3510=EDGE_CURVE ( 'NONE', #13184, #15860, #14228, .T. ) ;
#3537=DIRECTION ( 'NONE',  ( 0.000000000000000000, 0.5000000000000018874, 0.8660254037844374864 ) ) ;
#3554=AXIS2_PLACEMENT_3D ( 'NONE', #9157, #20102, #12316 ) ;
#3570=ORIENTED_EDGE ( 'NONE', *, *, #121, .F. ) ;
#3575=CARTESIAN_POINT ( 'NONE',  ( 7.350000000000000533, 9.000000000000000000, 0.000000000000000000 ) ) ;
#3587=CYLINDRICAL_SURFACE ( 'NONE', #15495, 9.000000000000001776 ) ;
#3600=ORIENTED_EDGE ( 'NONE', *, *, #5903, .F. ) ;
#3668=EDGE_CURVE ( 'NONE', #8563, #16678, #18198, .T. ) ;
#3705=CARTESIAN_POINT ( 'NONE',  ( 0.3570196857253503664, 9.540868182094907723, 1.474731560294323396 ) ) ;
#3709=CARTESIAN_POINT ( 'NONE',  ( 7.350000000000001421, -7.794228634059936489, 4.500000000000017764 ) ) ;
#3718=B_SPLINE_CURVE_WITH_KNOTS ( 'NONE', 3,
 ( #12826, #12728, #14064, #4970, #14373, #349 ),
 .UNSPECIFIED., .F., .F.,
 ( 4, 2, 4 ),
 ( 2.380730970505090493E-07, 0.002629065763328468884, 0.005257893453559887159 ),
 .UNSPECIFIED. ) ;
#3734=VERTEX_POINT ( 'NONE', #10610 ) ;
#3751=CARTESIAN_POINT ( 'NONE',  ( 0.8038475772933695307, 10.39230484541327471, -5.094467845664485666E-17 ) ) ;
#3798=SURFACE_SIDE_STYLE ('',( #12906 ) ) ;
#3810=PLANE ( 'NONE',  #13883 ) ;
#3816=ORIENTED_EDGE ( 'NONE', *, *, #18532, .T. ) ;
#3817=B_SPLINE_CURVE_WITH_KNOTS ( 'NONE', 3,
 ( #17063, #10702, #9386, #6020, #16958, #9176, #12237, #3151 ),
 .UNSPECIFIED., .F., .F.,
 ( 4, 2, 2, 4 ),
 ( 0.005257893453559910578, 0.006567392922673243386, 0.007876892391786575326, 0.01049589133001324268 ),
 .UNSPECIFIED. ) ;
#3832=AXIS2_PLACEMENT_3D ( 'NONE', #7639, #6229, #2846 ) ;
#3834=ORIENTED_EDGE ( 'NONE', *, *, #6019, .F. ) ;
#3862=DIRECTION ( 'NONE',  ( 1.000000000000000000, 0.000000000000000000, 0.000000000000000000 ) ) ;
#3872=DIRECTION ( 'NONE',  ( 1.000000000000000000, 0.000000000000000000, -0.000000000000000000 ) ) ;
#3925=ORIENTED_EDGE ( 'NONE', *, *, #6550, .F. ) ;
#3958=LINE ( 'NONE', #8469, #17102 ) ;
#3960=EDGE_LOOP ( 'NONE', ( #7313, #3816, #17135, #10126 ) ) ;
#3992=CARTESIAN_POINT ( 'NONE',  ( 7.950000000000000178, 5.196152422706624030, -9.000000000000001776 ) ) ;
#4005=CARTESIAN_POINT ( 'NONE',  ( 0.000000000000000000, 0.000000000000000000, 0.000000000000000000 ) ) ;
#4007=VECTOR ( 'NONE', #14949, 1000.000000000000000 ) ;
#4009=ADVANCED_FACE ( 'NONE', ( #17693, #2136 ), #1160, .T. ) ;
#4043=CIRCLE ( 'NONE', #13845, 9.000000000000001776 ) ;
#4044=CARTESIAN_POINT ( 'NONE',  ( 7.350000000000000533, 5.196152422706624030, -9.000000000000001776 ) ) ;
#4105=DIRECTION ( 'NONE',  ( -0.000000000000000000, 0.5000000000000012212, 0.8660254037844379305 ) ) ;
#4110=ORIENTED_EDGE ( 'NONE', *, *, #18588, .F. ) ;
#4116=AXIS2_PLACEMENT_3D ( 'NONE', #15583, #9446, #12601 ) ;
#4131=AXIS2_PLACEMENT_3D ( 'NONE', #10121, #8972, #18193 ) ;
#4143=FACE_OUTER_BOUND ( 'NONE', #16593, .T. ) ;
#4146=CARTESIAN_POINT ( 'NONE',  ( -1.148576676476831260E-14, -8.236864015571811137, 3.733333029993802565 ) ) ;
#4149=DIRECTION ( 'NONE',  ( -1.000000000000000000, -0.000000000000000000, -0.000000000000000000 ) ) ;
#4159=CARTESIAN_POINT ( 'NONE',  ( 0.000000000000000000, 0.000000000000000000, 0.000000000000000000 ) ) ;
#4161=EDGE_CURVE ( 'NONE', #19269, #13184, #6797, .T. ) ;
#4165=ORIENTED_EDGE ( 'NONE', *, *, #17691, .F. ) ;
#4168=VECTOR ( 'NONE', #13921, 1000.000000000000000 ) ;
#4193=VERTEX_POINT ( 'NONE', #13018 ) ;
#4225=VECTOR ( 'NONE', #17458, 1000.000000000000000 ) ;
#4251=CARTESIAN_POINT ( 'NONE',  ( 0.000000000000000000, 7.794228634059940930, -4.500000000000011546 ) ) ;
#4257=ORIENTED_EDGE ( 'NONE', *, *, #656, .T. ) ;
#4342=DIRECTION ( 'NONE',  ( -1.000000000000000000, -0.000000000000000000, -0.000000000000000000 ) ) ;
#4353=UNCERTAINTY_MEASURE_WITH_UNIT (LENGTH_MEASURE( 1.000000000000000082E-05 ), #8097, 'distance_accuracy_value', 'NONE');
#4379=CIRCLE ( 'NONE', #12210, 9.000000000000000000 ) ;
#4392=EDGE_CURVE ( 'NONE', #16678, #15182, #2294, .T. ) ;
#4434=CARTESIAN_POINT ( 'NONE',  ( 7.350000000000000533, 5.196152422706627583, 9.000000000000001776 ) ) ;
#4451=CYLINDRICAL_SURFACE ( 'NONE', #3554, 9.000000000000001776 ) ;
#4467=DIRECTION ( 'NONE',  ( 0.000000000000000000, 0.000000000000000000, -1.000000000000000000 ) ) ;
#4480=FACE_OUTER_BOUND ( 'NONE', #17088, .T. ) ;
#4509=PLANE ( 'NONE',  #13451 ) ;
#4511=CARTESIAN_POINT ( 'NONE',  ( 0.8038475772933646457, -10.39230484541326582, 2.804506490479260738E-17 ) ) ;
#4521=VECTOR ( 'NONE', #4814, 1000.000000000000114 ) ;
#4556=LINE ( 'NONE', #12214, #9738 ) ;
#4563=CARTESIAN_POINT ( 'NONE',  ( 0.000000000000000000, 0.000000000000000000, 0.000000000000000000 ) ) ;
#4572=EDGE_LOOP ( 'NONE', ( #7337, #19645, #8169, #13432 ) ) ;
#4584=CARTESIAN_POINT ( 'NONE',  ( -4.459628467293889707E-15, 7.573738413550457516, -4.881900264494500874 ) ) ;
#4590=CARTESIAN_POINT ( 'NONE',  ( 0.000000000000000000, 7.794228634059940930, -4.500000000000011546 ) ) ;
#4611=EDGE_CURVE ( 'NONE', #6828, #18284, #8907, .T. ) ;
#4670=DIRECTION ( 'NONE',  ( 0.000000000000000000, 0.000000000000000000, -1.000000000000000000 ) ) ;
#4689=CARTESIAN_POINT ( 'NONE',  ( 62.95000000000000284, 6.757601037695096551E-16, -5.035999999999999588 ) ) ;
#4712=CIRCLE ( 'NONE', #6012, 9.000000000000000000 ) ;
#4789=DIRECTION ( 'NONE',  ( 0.000000000000000000, 0.000000000000000000, -1.000000000000000000 ) ) ;
#4791=CARTESIAN_POINT ( 'NONE',  ( 7.350000000000001421, 0.000000000000000000, 0.000000000000000000 ) ) ;
#4814=DIRECTION ( 'NONE',  ( -0.000000000000000000, 0.5000000000000012212, 0.8660254037844379305 ) ) ;
#4944=ORIENTED_EDGE ( 'NONE', *, *, #14517, .F. ) ;
#4970=CARTESIAN_POINT ( 'NONE',  ( 0.07661102881317106983, -6.914460432017385472, -6.023803224821242530 ) ) ;
#4986=ORIENTED_EDGE ( 'NONE', *, *, #6188, .T. ) ;
#5059=DIRECTION ( 'NONE',  ( -1.000000000000000000, -0.000000000000000000, 0.000000000000000000 ) ) ;
#5106=CARTESIAN_POINT ( 'NONE',  ( 7.350000000000000533, -10.39230484541326582, 0.000000000000000000 ) ) ;
#5141=CIRCLE ( 'NONE', #2198, 9.000000000000001776 ) ;
#5144=ORIENTED_EDGE ( 'NONE', *, *, #3668, .T. ) ;
#5153=EDGE_CURVE ( 'NONE', #5943, #7173, #3958, .T. ) ;
#5164=DIRECTION ( 'NONE',  ( 0.000000000000000000, 0.000000000000000000, -1.000000000000000000 ) ) ;
#5173=EDGE_CURVE ( 'NONE', #16123, #4193, #15691, .T. ) ;
#5179=EDGE_CURVE ( 'NONE', #16678, #4193, #885, .T. ) ;
#5180=DIRECTION ( 'NONE',  ( 0.000000000000000000, 0.000000000000000000, 1.000000000000000000 ) ) ;
#5183=CARTESIAN_POINT ( 'NONE',  ( 7.950000000000000178, -10.39230484541326582, 0.000000000000000000 ) ) ;
#5208=DIRECTION ( 'NONE',  ( 0.000000000000000000, -0.5000000000000009992, 0.8660254037844380415 ) ) ;
#5220=B_SPLINE_CURVE_WITH_KNOTS ( 'NONE', 3,
 ( #8968, #4584, #10708, #16962, #15210, #12341, #2953, #18397 ),
 .UNSPECIFIED., .F., .F.,
 ( 4, 2, 2, 4 ),
 ( 0.005257893453559907108, 0.006567392922673239916, 0.007876892391786571856, 0.01049589133001323747 ),
 .UNSPECIFIED. ) ;
#5222=CARTESIAN_POINT ( 'NONE',  ( 0.09252763182292003674, -8.674330214978045461, -2.975619346028160805 ) ) ;
#5260=ADVANCED_FACE ( 'NONE', ( #10004 ), #14706, .T. ) ;
#5261=DIRECTION ( 'NONE',  ( 0.000000000000000000, -0.5000000000000009992, 0.8660254037844380415 ) ) ;
#5263=ADVANCED_FACE ( 'NONE', ( #11917 ), #3140, .T. ) ;
#5275=AXIS2_PLACEMENT_3D ( 'NONE', #13445, #5695, #13964 ) ;
#5295=EDGE_LOOP ( 'NONE', ( #1030, #11317, #13331 ) ) ;
#5307=CARTESIAN_POINT ( 'NONE',  ( -1.067261513540418057E-16, -0.8794428697894906000, -9.000000000000000000 ) ) ;
#5309=ORIENTED_EDGE ( 'NONE', *, *, #10759, .F. ) ;
#5314=PLANE ( 'NONE',  #7137 ) ;
#5354=FACE_OUTER_BOUND ( 'NONE', #18962, .T. ) ;
#5370=EDGE_LOOP ( 'NONE', ( #12508, #1431 ) ) ;
#5401=DIRECTION ( 'NONE',  ( 1.000000000000000000, 0.000000000000000000, 0.000000000000000000 ) ) ;
#5409=PLANE ( 'NONE',  #19069 ) ;
#5411=DIRECTION ( 'NONE',  ( 1.000000000000000000, 0.000000000000000000, 0.000000000000000000 ) ) ;
#5439=ORIENTED_EDGE ( 'NONE', *, *, #656, .F. ) ;
#5456=ORIENTED_EDGE ( 'NONE', *, *, #19496, .T. ) ;
#5585=DIRECTION ( 'NONE',  ( 1.000000000000000000, 0.000000000000000000, 0.000000000000000000 ) ) ;
#5602=CARTESIAN_POINT ( 'NONE',  ( 62.95000000000000284, 0.000000000000000000, 0.000000000000000000 ) ) ;
#5638=EDGE_CURVE ( 'NONE', #3301, #10259, #9069, .T. ) ;
#5656=CONICAL_SURFACE ( 'NONE', #16440, 9.000000000000000000, 1.047197551196600296 ) ;
#5664=CARTESIAN_POINT ( 'NONE',  ( 7.350000000000000533, 5.196152422706627583, 9.000000000000001776 ) ) ;
#5668=ORIENTED_EDGE ( 'NONE', *, *, #13265, .F. ) ;
#5684=CARTESIAN_POINT ( 'NONE',  ( 62.95000000000000284, 0.000000000000000000, 0.000000000000000000 ) ) ;
#5690=DIRECTION ( 'NONE',  ( 0.000000000000000000, 0.000000000000000000, -1.000000000000000000 ) ) ;
#5695=DIRECTION ( 'NONE',  ( 1.000000000000000000, 0.000000000000000000, -0.000000000000000000 ) ) ;
#5699=ORIENTED_EDGE ( 'NONE', *, *, #16613, .F. ) ;
#5707=AXIS2_PLACEMENT_3D ( 'NONE', #9737, #11275, #12497 ) ;
#5742=EDGE_CURVE ( 'NONE', #19269, #2533, #10638, .T. ) ;
#5763=AXIS2_PLACEMENT_3D ( 'NONE', #7515, #13957, #20200 ) ;
#5824=AXIS2_PLACEMENT_3D ( 'NONE', #13749, #4342, #18264 ) ;
#5863=ORIENTED_EDGE ( 'NONE', *, *, #11979, .T. ) ;
#5877=LINE ( 'NONE', #4434, #9520 ) ;
#5882=DIRECTION ( 'NONE',  ( 1.000000000000000000, 0.000000000000000000, -0.000000000000000000 ) ) ;
#5903=EDGE_CURVE ( 'NONE', #15182, #12589, #2902, .T. ) ;
#5909=ORIENTED_EDGE ( 'NONE', *, *, #10008, .F. ) ;
#5913=FACE_OUTER_BOUND ( 'NONE', #2803, .T. ) ;
#5931=EDGE_LOOP ( 'NONE', ( #6221, #6036, #12966 ) ) ;
#5943=VERTEX_POINT ( 'NONE', #12499 ) ;
#5972=ORIENTED_EDGE ( 'NONE', *, *, #17806, .F. ) ;
#5984=CIRCLE ( 'NONE', #18068, 5.035999999999999588 ) ;
#6012=AXIS2_PLACEMENT_3D ( 'NONE', #3001, #9230, #12291 ) ;
#6019=EDGE_CURVE ( 'NONE', #15218, #14685, #8036, .T. ) ;
#6020=CARTESIAN_POINT ( 'NONE',  ( 0.09252763182291320887, -6.914127053141824852, 6.024380653971842747 ) ) ;
#6036=ORIENTED_EDGE ( 'NONE', *, *, #14975, .T. ) ;
#6062=DIRECTION ( 'NONE',  ( 0.000000000000000000, 0.000000000000000000, -1.000000000000000000 ) ) ;
#6067=( GEOMETRIC_REPRESENTATION_CONTEXT ( 3 ) GLOBAL_UNCERTAINTY_ASSIGNED_CONTEXT ( ( #4353 ) ) GLOBAL_UNIT_ASSIGNED_CONTEXT ( ( #8097, #9837, #17534 ) ) REPRESENTATION_CONTEXT ( 'NONE', 'WORKASPACE' ) );
#6149=LINE ( 'NONE', #16880, #12184 ) ;
#6173=ORIENTED_EDGE ( 'NONE', *, *, #3510, .F. ) ;
#6188=EDGE_CURVE ( 'NONE', #10259, #12149, #14597, .T. ) ;
#6191=VECTOR ( 'NONE', #17880, 1000.000000000000000 ) ;
#6220=ORIENTED_EDGE ( 'NONE', *, *, #6550, .T. ) ;
#6221=ORIENTED_EDGE ( 'NONE', *, *, #17739, .T. ) ;
#6225=DIRECTION ( 'NONE',  ( -1.000000000000000000, -0.000000000000000000, -0.000000000000000000 ) ) ;
#6229=DIRECTION ( 'NONE',  ( -1.000000000000000000, -0.000000000000000000, -0.000000000000000000 ) ) ;
#6255=ADVANCED_FACE ( 'NONE', ( #4480 ), #3261, .F. ) ;
#6276=( NAMED_UNIT ( * ) SI_UNIT ( $, .STERADIAN. ) SOLID_ANGLE_UNIT ( ) );
#6317=VERTEX_POINT ( 'NONE', #14200 ) ;
#6351=ORIENTED_EDGE ( 'NONE', *, *, #5742, .F. ) ;
#6407=DIRECTION ( 'NONE',  ( -0.7071067811865516806, 8.659560562354883554E-17, -0.7071067811865434649 ) ) ;
#6451=CARTESIAN_POINT ( 'NONE',  ( 7.950000000000000178, 1.102182119232617911E-15, -9.000000000000001776 ) ) ;
#6480=ORIENTED_EDGE ( 'NONE', *, *, #12258, .T. ) ;
#6530=LINE ( 'NONE', #1614, #7709 ) ;
#6544=AXIS2_PLACEMENT_3D ( 'NONE', #8848, #13650, #2719 ) ;
#6550=EDGE_CURVE ( 'NONE', #7508, #15218, #13692, .T. ) ;
#6566=DIRECTION ( 'NONE',  ( -1.000000000000000000, -0.000000000000000000, -0.000000000000000000 ) ) ;
#6570=CARTESIAN_POINT ( 'NONE',  ( 7.950000000000000178, 5.196152422706627583, 9.000000000000001776 ) ) ;
#6590=DIRECTION ( 'NONE',  ( 0.000000000000000000, 0.000000000000000000, -1.000000000000000000 ) ) ;
#6686=FILL_AREA_STYLE ('',( #1975 ) ) ;
#6695=CARTESIAN_POINT ( 'NONE',  ( 0.000000000000000000, 0.000000000000000000, 0.000000000000000000 ) ) ;
#6737=DIRECTION ( 'NONE',  ( 0.000000000000000000, 0.000000000000000000, 1.000000000000000000 ) ) ;
#6741=ORIENTED_EDGE ( 'NONE', *, *, #10759, .T. ) ;
#6748=ORIENTED_EDGE ( 'NONE', *, *, #4611, .F. ) ;
#6797=LINE ( 'NONE', #12817, #8242 ) ;
#6799=CIRCLE ( 'NONE', #3832, 6.000000000000001776 ) ;
#6828=VERTEX_POINT ( 'NONE', #12832 ) ;
#6835=DIRECTION ( 'NONE',  ( 0.000000000000000000, 0.000000000000000000, -1.000000000000000000 ) ) ;
#6937=EDGE_LOOP ( 'NONE', ( #12236, #19592, #7688 ) ) ;
#6972=DIRECTION ( 'NONE',  ( -0.000000000000000000, 3.338476886082577323E-16, 1.000000000000000000 ) ) ;
#6986=ORIENTED_EDGE ( 'NONE', *, *, #13640, .T. ) ;
#7002=CYLINDRICAL_SURFACE ( 'NONE', #1612, 6.000000000000001776 ) ;
#7032=CIRCLE ( 'NONE', #10272, 9.000000000000000000 ) ;
#7040=CARTESIAN_POINT ( 'NONE',  ( 0.3552109633508538367, -3.484997970623676444, -8.999999999999998224 ) ) ;
#7085=EDGE_CURVE ( 'NONE', #18284, #6828, #2685, .T. ) ;
#7137=AXIS2_PLACEMENT_3D ( 'NONE', #19431, #5411, #19330 ) ;
#7173=VERTEX_POINT ( 'NONE', #3709 ) ;
#7177=CARTESIAN_POINT ( 'NONE',  ( 7.950000000000000178, 0.000000000000000000, 0.000000000000000000 ) ) ;
#7188=ORIENTED_EDGE ( 'NONE', *, *, #16613, .T. ) ;
#7224=CARTESIAN_POINT ( 'NONE',  ( 0.3563104543936381208, 9.539178283403856540, -1.477658550686872907 ) ) ;
#7245=EDGE_LOOP ( 'NONE', ( #2994, #1504, #2360, #18314, #5439, #3600 ) ) ;
#7248=CARTESIAN_POINT ( 'NONE',  ( 1.355252715606880851E-17, 0.4400770685579600827, 9.000000000000000000 ) ) ;
#7278=ADVANCED_FACE ( 'NONE', ( #9105 ), #4509, .F. ) ;
#7310=PLANE ( 'NONE',  #1784 ) ;
#7313=ORIENTED_EDGE ( 'NONE', *, *, #13994, .T. ) ;
#7337=ORIENTED_EDGE ( 'NONE', *, *, #18532, .F. ) ;
#7401=CARTESIAN_POINT ( 'NONE',  ( 7.950000000000000178, 10.39230484541327471, -5.498853076140229456E-16 ) ) ;
#7470=CARTESIAN_POINT ( 'NONE',  ( 0.3552109633508171438, -3.484997970623485930, 8.999999999999998224 ) ) ;
#7508=VERTEX_POINT ( 'NONE', #12686 ) ;
#7512=DIRECTION ( 'NONE',  ( -1.000000000000000000, 0.000000000000000000, -0.000000000000000000 ) ) ;
#7515=CARTESIAN_POINT ( 'NONE',  ( 7.350000000000001421, 0.000000000000000000, 0.000000000000000000 ) ) ;
#7519=CARTESIAN_POINT ( 'NONE',  ( 0.07661102881317853608, 8.673996836102551455, -2.976196775178697962 ) ) ;
#7604=VERTEX_POINT ( 'NONE', #12887 ) ;
#7608=FACE_OUTER_BOUND ( 'NONE', #5370, .T. ) ;
#7613=AXIS2_PLACEMENT_3D ( 'NONE', #5684, #16826, #15286 ) ;
#7639=CARTESIAN_POINT ( 'NONE',  ( 61.98599999999999000, 0.000000000000000000, 0.000000000000000000 ) ) ;
#7655=ORIENTED_EDGE ( 'NONE', *, *, #12660, .T. ) ;
#7688=ORIENTED_EDGE ( 'NONE', *, *, #11972, .T. ) ;
#7709=VECTOR ( 'NONE', #11111, 1000.000000000000000 ) ;
#7783=DIRECTION ( 'NONE',  ( 1.000000000000000000, 0.000000000000000000, 0.000000000000000000 ) ) ;
#7802=CYLINDRICAL_SURFACE ( 'NONE', #5707, 6.000000000000001776 ) ;
#7949=CARTESIAN_POINT ( 'NONE',  ( 0.8038475772933632024, 5.196152422706628471, 9.000000000000001776 ) ) ;
#7971=VERTEX_POINT ( 'NONE', #17115 ) ;
#8036=CIRCLE ( 'NONE', #4116, 9.000000000000000000 ) ;
#8043=ORIENTED_EDGE ( 'NONE', *, *, #15676, .F. ) ;
#8063=MANIFOLD_SOLID_BREP ( 'BearingFace', #9352 ) ;
#8077=DIRECTION ( 'NONE',  ( 0.000000000000000000, 0.000000000000000000, 1.000000000000000000 ) ) ;
#8086=CARTESIAN_POINT ( 'NONE',  ( 7.950000000000000178, 0.000000000000000000, 0.000000000000000000 ) ) ;
#8097=( LENGTH_UNIT ( ) NAMED_UNIT ( * ) SI_UNIT ( .MILLI., .METRE. ) );
#8120=ADVANCED_FACE ( 'NONE', ( #3503 ), #19646, .F. ) ;
#8129=AXIS2_PLACEMENT_3D ( 'NONE', #14176, #18992, #5180 ) ;
#8142=EDGE_LOOP ( 'NONE', ( #907, #15153 ) ) ;
#8153=ORIENTED_EDGE ( 'NONE', *, *, #14975, .F. ) ;
#8169=ORIENTED_EDGE ( 'NONE', *, *, #12501, .T. ) ;
#8242=VECTOR ( 'NONE', #5261, 1000.000000000000000 ) ;
#8246=EDGE_CURVE ( 'NONE', #12149, #3301, #14736, .T. ) ;
#8305=DIRECTION ( 'NONE',  ( 0.000000000000000000, 0.000000000000000000, 1.000000000000000000 ) ) ;
#8341=EDGE_LOOP ( 'NONE', ( #5456, #2078, #4944 ) ) ;
#8343=AXIS2_PLACEMENT_3D ( 'NONE', #3992, #6972, #11855 ) ;
#8350=ORIENTED_EDGE ( 'NONE', *, *, #10008, .T. ) ;
#8361=PLANE ( 'NONE',  #9723 ) ;
#8367=CARTESIAN_POINT ( 'NONE',  ( 0.000000000000000000, -3.004629197474319246E-15, -9.000000000000000000 ) ) ;
#8394=PRODUCT_DEFINITION ( 'UNKNOWN', '', #2021, #10918 ) ;
#8416=CARTESIAN_POINT ( 'NONE',  ( 0.000000000000000000, 0.000000000000000000, 0.000000000000000000 ) ) ;
#8459=CARTESIAN_POINT ( 'NONE',  ( 0.000000000000000000, 0.000000000000000000, 9.000000000000001776 ) ) ;
#8462=LINE ( 'NONE', #13248, #18565 ) ;
#8469=CARTESIAN_POINT ( 'NONE',  ( 7.350000000000000533, -10.39230484541326582, 0.000000000000000000 ) ) ;
#8475=EDGE_CURVE ( 'NONE', #15218, #3734, #5220, .T. ) ;
#8501=B_SPLINE_CURVE_WITH_KNOTS ( 'NONE', 3,
 ( #15610, #7248, #15403, #18473, #10685, #13862, #1391, #15021 ),
 .UNSPECIFIED., .F., .F.,
 ( 4, 2, 2, 4 ),
 ( 0.01498083277331294441, 0.01629713195395221526, 0.01761343113459148957, 0.02024602949587003126 ),
 .UNSPECIFIED. ) ;
#8515=CARTESIAN_POINT ( 'NONE',  ( 0.000000000000000000, 7.794228634059941818, 4.500000000000007994 ) ) ;
#8563=VERTEX_POINT ( 'NONE', #15732 ) ;
#8620=ORIENTED_EDGE ( 'NONE', *, *, #5742, .T. ) ;
#8698=DIRECTION ( 'NONE',  ( 1.000000000000000000, 0.000000000000000000, -0.000000000000000000 ) ) ;
#8723=ADVANCED_FACE ( 'NONE', ( #3505 ), #7802, .T. ) ;
#8745=CARTESIAN_POINT ( 'NONE',  ( 0.5584673446549131004, -9.967293815311094818, 0.7361406979141402740 ) ) ;
#8766=VECTOR ( 'NONE', #6407, 1000.000000000000000 ) ;
#8779=AXIS2_PLACEMENT_3D ( 'NONE', #4563, #17048, #4670 ) ;
#8835=ORIENTED_EDGE ( 'NONE', *, *, #8246, .T. ) ;
#8843=PLANE ( 'NONE',  #19426 ) ;
#8848=CARTESIAN_POINT ( 'NONE',  ( 62.95000000000000284, 0.000000000000000000, 0.000000000000000000 ) ) ;
#8907=CIRCLE ( 'NONE', #16433, 6.000000000000001776 ) ;
#8921=CARTESIAN_POINT ( 'NONE',  ( 7.350000000000001421, 0.000000000000000000, 9.000000000000000000 ) ) ;
#8938=ORIENTED_EDGE ( 'NONE', *, *, #15342, .T. ) ;
#8945=CARTESIAN_POINT ( 'NONE',  ( 0.000000000000000000, 0.000000000000000000, 0.000000000000000000 ) ) ;
#8968=CARTESIAN_POINT ( 'NONE',  ( 0.000000000000000000, 7.794228634059940930, -4.500000000000011546 ) ) ;
#8972=DIRECTION ( 'NONE',  ( 1.000000000000000000, 0.000000000000000000, -0.000000000000000000 ) ) ;
#8990=AXIS2_PLACEMENT_3D ( 'NONE', #4159, #13662, #15304 ) ;
#9006=EDGE_LOOP ( 'NONE', ( #18104, #1184, #13874 ) ) ;
#9025=CARTESIAN_POINT ( 'NONE',  ( 0.000000000000000000, -7.794228634059936489, 4.500000000000017764 ) ) ;
#9069=B_SPLINE_CURVE_WITH_KNOTS ( 'NONE', 3,
 ( #2516, #8745, #14989, #18164, #4146, #16635 ),
 .UNSPECIFIED., .F., .F.,
 ( 4, 2, 4 ),
 ( 2.380730968224042413E-07, 0.002629065763328366535, 0.005257893453559910578 ),
 .UNSPECIFIED. ) ;
#9105=FACE_OUTER_BOUND ( 'NONE', #2649, .T. ) ;
#9139=ORIENTED_EDGE ( 'NONE', *, *, #15416, .F. ) ;
#9157=CARTESIAN_POINT ( 'NONE',  ( 0.000000000000000000, 0.000000000000000000, 0.000000000000000000 ) ) ;
#9176=CARTESIAN_POINT ( 'NONE',  ( 0.3570196857253401523, -6.047589086024969696, 7.525268439705683932 ) ) ;
#9184=DIRECTION ( 'NONE',  ( 1.000000000000000000, 0.000000000000000000, -0.000000000000000000 ) ) ;
#9230=DIRECTION ( 'NONE',  ( -1.000000000000000000, -0.000000000000000000, -0.000000000000000000 ) ) ;
#9346=EDGE_CURVE ( 'NONE', #15860, #14685, #15744, .T. ) ;
#9352=CLOSED_SHELL ( 'NONE', ( #14955, #12751, #8723, #4009, #18661, #9730, #1376, #1542, #11651, #13454, #13509, #5260, #17413, #18480, #6255, #13588, #5263, #11014, #17863, #9657, #15655, #8120, #2926, #19659, #15607, #7278, #1480 ) ) ;
#9386=CARTESIAN_POINT ( 'NONE',  ( 0.01899995639452935550, -7.352259170992699211, 5.265513565426384268 ) ) ;
#9431=VERTEX_POINT ( 'NONE', #3157 ) ;
#9446=DIRECTION ( 'NONE',  ( 1.000000000000000000, 0.000000000000000000, -0.000000000000000000 ) ) ;
#9517=CARTESIAN_POINT ( 'NONE',  ( 0.000000000000000000, -7.794228634059948035, -4.499999999999999112 ) ) ;
#9520=VECTOR ( 'NONE', #18768, 1000.000000000000000 ) ;
#9568=CARTESIAN_POINT ( 'NONE',  ( 0.000000000000000000, 1.102182119232617911E-15, -9.000000000000001776 ) ) ;
#9592=CARTESIAN_POINT ( 'NONE',  ( -3.391519920806218558E-15, 7.351593252548065394, 5.266666970006217419 ) ) ;
#9641=CARTESIAN_POINT ( 'NONE',  ( 0.8038475772933695307, 10.39230484541327471, -5.094467845664485666E-17 ) ) ;
#9657=ADVANCED_FACE ( 'NONE', ( #19502 ), #17629, .T. ) ;
#9665=LINE ( 'NONE', #9568, #4225 ) ;
#9712=CARTESIAN_POINT ( 'NONE',  ( 0.000000000000000000, 0.000000000000000000, 6.000000000000001776 ) ) ;
#9723=AXIS2_PLACEMENT_3D ( 'NONE', #14607, #5401, #6835 ) ;
#9730=ADVANCED_FACE ( 'NONE', ( #10373 ), #20237, .T. ) ;
#9737=CARTESIAN_POINT ( 'NONE',  ( 0.000000000000000000, 0.000000000000000000, 0.000000000000000000 ) ) ;
#9738=VECTOR ( 'NONE', #15394, 1000.000000000000114 ) ;
#9837=( NAMED_UNIT ( * ) PLANE_ANGLE_UNIT ( ) SI_UNIT ( $, .RADIAN. ) );
#9838=CARTESIAN_POINT ( 'NONE',  ( 0.000000000000000000, 0.000000000000000000, 0.000000000000000000 ) ) ;
#9847=DIRECTION ( 'NONE',  ( 0.000000000000000000, 3.338476886082585705E-16, -1.000000000000000000 ) ) ;
#9862=CARTESIAN_POINT ( 'NONE',  ( 0.5612050131687996712, 4.355613924421553484, -9.000000000000001776 ) ) ;
#9913=DIRECTION ( 'NONE',  ( 0.000000000000000000, 0.000000000000000000, -1.000000000000000000 ) ) ;
#9924=FACE_OUTER_BOUND ( 'NONE', #20101, .T. ) ;
#9966=CARTESIAN_POINT ( 'NONE',  ( 6.352747104407250078E-17, 0.4400770685579608044, -9.000000000000000000 ) ) ;
#9979=ORIENTED_EDGE ( 'NONE', *, *, #11979, .F. ) ;
#9980=EDGE_CURVE ( 'NONE', #3734, #16123, #16215, .T. ) ;
#10004=FACE_OUTER_BOUND ( 'NONE', #17864, .T. ) ;
#10008=EDGE_CURVE ( 'NONE', #13410, #15182, #9665, .T. ) ;
#10107=DIRECTION ( 'NONE',  ( 0.000000000000000000, 0.000000000000000000, -1.000000000000000000 ) ) ;
#10111=DIRECTION ( 'NONE',  ( 1.000000000000000000, 0.000000000000000000, 0.000000000000000000 ) ) ;
#10121=CARTESIAN_POINT ( 'NONE',  ( 0.000000000000000000, 0.000000000000000000, 0.000000000000000000 ) ) ;
#10126=ORIENTED_EDGE ( 'NONE', *, *, #12501, .F. ) ;
#10134=ORIENTED_EDGE ( 'NONE', *, *, #4611, .T. ) ;
#10153=DIRECTION ( 'NONE',  ( 0.000000000000000000, 0.000000000000000000, -1.000000000000000000 ) ) ;
#10176=VERTEX_POINT ( 'NONE', #11883 ) ;
#10227=MECHANICAL_DESIGN_GEOMETRIC_PRESENTATION_REPRESENTATION('',(#11848),#6067);
#10259=VERTEX_POINT ( 'NONE', #9025 ) ;
#10272=AXIS2_PLACEMENT_3D ( 'NONE', #85, #491, #6737 ) ;
#10324=DIRECTION ( 'NONE',  ( 0.000000000000000000, 0.000000000000000000, -1.000000000000000000 ) ) ;
#10343=ORIENTED_EDGE ( 'NONE', *, *, #15676, .T. ) ;
#10373=FACE_OUTER_BOUND ( 'NONE', #4572, .T. ) ;
#10603=CARTESIAN_POINT ( 'NONE',  ( 0.000000000000000000, 10.39230484541327471, -5.498853076140229456E-16 ) ) ;
#10610=CARTESIAN_POINT ( 'NONE',  ( 0.8038475772933615371, 5.196152422706624030, -9.000000000000001776 ) ) ;
#10624=ORIENTED_EDGE ( 'NONE', *, *, #9346, .F. ) ;
#10638=CIRCLE ( 'NONE', #5763, 9.000000000000000000 ) ;
#10685=CARTESIAN_POINT ( 'NONE',  ( 0.1482032042127255644, 2.204400401860219905, 9.000000000000001776 ) ) ;
#10702=CARTESIAN_POINT ( 'NONE',  ( -1.140219284730587620E-14, -7.573738413550444193, 4.881900264494501762 ) ) ;
#10708=CARTESIAN_POINT ( 'NONE',  ( 0.01899995639453595439, 7.352259170992715198, -5.265513565426385156 ) ) ;
#10741=CARTESIAN_POINT ( 'NONE',  ( 7.950000000000000178, 10.39230484541327471, 0.000000000000000000 ) ) ;
#10759=EDGE_CURVE ( 'NONE', #10176, #13146, #14798, .T. ) ;
#10784=DIRECTION ( 'NONE',  ( -0.000000000000000000, 0.000000000000000000, 1.000000000000000000 ) ) ;
#10816=CARTESIAN_POINT ( 'NONE',  ( 7.350000000000001421, -3.004629197474319640E-15, -9.000000000000001776 ) ) ;
#10918=PRODUCT_DEFINITION_CONTEXT ( 'detailed design', #18620, 'design' ) ;
#10974=CARTESIAN_POINT ( 'NONE',  ( 7.950000000000000178, -5.196152422706636465, -8.999999999999998224 ) ) ;
#11014=ADVANCED_FACE ( 'NONE', ( #14178 ), #1278, .T. ) ;
#11035=AXIS2_PLACEMENT_3D ( 'NONE', #4005, #11968, #10153 ) ;
#11111=DIRECTION ( 'NONE',  ( -1.000000000000000000, -0.000000000000000000, -0.000000000000000000 ) ) ;
#11144=LINE ( 'NONE', #15475, #2993 ) ;
#11199=FACE_OUTER_BOUND ( 'NONE', #16550, .T. ) ;
#11251=CARTESIAN_POINT ( 'NONE',  ( 7.350000000000001421, 7.794228634059941818, 4.500000000000007994 ) ) ;
#11275=DIRECTION ( 'NONE',  ( -1.000000000000000000, -0.000000000000000000, -0.000000000000000000 ) ) ;
#11287=ORIENTED_EDGE ( 'NONE', *, *, #8475, .T. ) ;
#11317=ORIENTED_EDGE ( 'NONE', *, *, #149, .T. ) ;
#11496=CARTESIAN_POINT ( 'NONE',  ( 0.3593302862868668068, 3.504574740656555498, -9.000000000000000000 ) ) ;
#11522=VECTOR ( 'NONE', #18329, 1000.000000000000000 ) ;
#11542=PLANE ( 'NONE',  #14158 ) ;
#11575=CARTESIAN_POINT ( 'NONE',  ( -3.428789370485404223E-15, 8.014718854569430562, 4.118099735505520442 ) ) ;
#11651=ADVANCED_FACE ( 'NONE', ( #14421 ), #5314, .T. ) ;
#11669=ORIENTED_EDGE ( 'NONE', *, *, #17691, .T. ) ;
#11698=CONICAL_SURFACE ( 'NONE', #20193, 9.000000000000000000, 1.047197551196600296 ) ;
#11708=DIRECTION ( 'NONE',  ( -0.7071067811865516806, 0.000000000000000000, 0.7071067811865434649 ) ) ;
#11788=VECTOR ( 'NONE', #12784, 1000.000000000000000 ) ;
#11819=DIRECTION ( 'NONE',  ( -1.000000000000000000, -0.000000000000000000, -0.000000000000000000 ) ) ;
#11848=STYLED_ITEM ( 'NONE', ( #19159 ), #8063 ) ;
#11855=DIRECTION ( 'NONE',  ( 0.000000000000000000, -1.000000000000000000, 3.338476886082577323E-16 ) ) ;
#11883=CARTESIAN_POINT ( 'NONE',  ( 7.950000000000000178, 0.000000000000000000, 9.000000000000001776 ) ) ;
#11909=CARTESIAN_POINT ( 'NONE',  ( 7.950000000000000178, 7.347880794884121708E-16, -6.000000000000001776 ) ) ;
#11917=FACE_OUTER_BOUND ( 'NONE', #8341, .T. ) ;
#11924=CARTESIAN_POINT ( 'NONE',  ( 0.5590800469813659301, 9.968355046870087222, 0.7343025909353927405 ) ) ;
#11968=DIRECTION ( 'NONE',  ( 1.000000000000000000, 0.000000000000000000, -0.000000000000000000 ) ) ;
#11972=EDGE_CURVE ( 'NONE', #13146, #19269, #15305, .T. ) ;
#11979=EDGE_CURVE ( 'NONE', #10259, #166, #3817, .T. ) ;
#12011=ORIENTED_EDGE ( 'NONE', *, *, #6188, .F. ) ;
#12063=CARTESIAN_POINT ( 'NONE',  ( 0.8038475772933556529, -5.196152422706607155, 8.999999999999998224 ) ) ;
#12066=EDGE_LOOP ( 'NONE', ( #5909, #15657, #6741, #9139, #556, #4110 ) ) ;
#12095=DIRECTION ( 'NONE',  ( -0.000000000000000000, 0.000000000000000000, -1.000000000000000000 ) ) ;
#12127=DIRECTION ( 'NONE',  ( 0.000000000000000000, 0.000000000000000000, 1.000000000000000000 ) ) ;
#12149=VERTEX_POINT ( 'NONE', #15208 ) ;
#12181=CIRCLE ( 'NONE', #746, 6.000000000000001776 ) ;
#12184=VECTOR ( 'NONE', #19838, 1000.000000000000000 ) ;
#12210=AXIS2_PLACEMENT_3D ( 'NONE', #9838, #2080, #8305 ) ;
#12214=CARTESIAN_POINT ( 'NONE',  ( 7.350000000000000533, -5.196152422706636465, -8.999999999999998224 ) ) ;
#12236=ORIENTED_EDGE ( 'NONE', *, *, #4161, .T. ) ;
#12237=CARTESIAN_POINT ( 'NONE',  ( 0.5590800469813547169, -5.620102221249795527, 8.265697409064612700 ) ) ;
#12258=EDGE_CURVE ( 'NONE', #6317, #2094, #6799, .T. ) ;
#12279=EDGE_LOOP ( 'NONE', ( #15599, #3294, #16871, #15352, #3497, #13230 ) ) ;
#12291=DIRECTION ( 'NONE',  ( 0.000000000000000000, 0.000000000000000000, 1.000000000000000000 ) ) ;
#12294=CIRCLE ( 'NONE', #1177, 9.000000000000000000 ) ;
#12311=FACE_OUTER_BOUND ( 'NONE', #3960, .T. ) ;
#12316=DIRECTION ( 'NONE',  ( 0.000000000000000000, 0.000000000000000000, 1.000000000000000000 ) ) ;
#12328=ORIENTED_EDGE ( 'NONE', *, *, #17392, .T. ) ;
#12341=CARTESIAN_POINT ( 'NONE',  ( 0.3570196857253458145, 6.047589086024989236, -7.525268439705685708 ) ) ;
#12345=UNCERTAINTY_MEASURE_WITH_UNIT (LENGTH_MEASURE( 1.000000000000000082E-05 ), #19961, 'distance_accuracy_value', 'NONE');
#12373=VECTOR ( 'NONE', #4149, 1000.000000000000000 ) ;
#12459=VERTEX_POINT ( 'NONE', #4689 ) ;
#12497=DIRECTION ( 'NONE',  ( 0.000000000000000000, 0.000000000000000000, 1.000000000000000000 ) ) ;
#12499=CARTESIAN_POINT ( 'NONE',  ( 7.350000000000000533, -5.196152422706607155, 8.999999999999998224 ) ) ;
#12501=EDGE_CURVE ( 'NONE', #7604, #2094, #19406, .T. ) ;
#12508=ORIENTED_EDGE ( 'NONE', *, *, #13994, .F. ) ;
#12552=CARTESIAN_POINT ( 'NONE',  ( 0.5584673446549148768, 5.621163452808795036, 8.263859302085863945 ) ) ;
#12589=VERTEX_POINT ( 'NONE', #4044 ) ;
#12601=DIRECTION ( 'NONE',  ( 0.000000000000000000, 0.000000000000000000, -1.000000000000000000 ) ) ;
#12635=ORIENTED_EDGE ( 'NONE', *, *, #15342, .F. ) ;
#12660=EDGE_CURVE ( 'NONE', #7971, #8563, #4556, .T. ) ;
#12686=CARTESIAN_POINT ( 'NONE',  ( 0.8038475772933695307, 10.39230484541327471, -5.094467845664485666E-17 ) ) ;
#12715=DIRECTION ( 'NONE',  ( 0.000000000000000000, 1.000000000000000000, 3.338476886082585705E-16 ) ) ;
#12728=CARTESIAN_POINT ( 'NONE',  ( 0.5584673446548692466, -5.621163452808894512, -8.263859302085696967 ) ) ;
#12732=CARTESIAN_POINT ( 'NONE',  ( 62.95000000000000284, 6.167321280506070407E-16, -5.035999999999999588 ) ) ;
#12745=ORIENTED_EDGE ( 'NONE', *, *, #17392, .F. ) ;
#12751=ADVANCED_FACE ( 'NONE', ( #12311 ), #15627, .T. ) ;
#12784=DIRECTION ( 'NONE',  ( -1.000000000000000000, -0.000000000000000000, -0.000000000000000000 ) ) ;
#12800=EDGE_LOOP ( 'NONE', ( #8043, #6480, #352, #502 ) ) ;
#12817=CARTESIAN_POINT ( 'NONE',  ( 7.350000000000000533, 10.39230484541327471, 0.000000000000000000 ) ) ;
#12826=CARTESIAN_POINT ( 'NONE',  ( 0.8038475772931082952, -5.196152422707021934, -8.999999999999998224 ) ) ;
#12832=CARTESIAN_POINT ( 'NONE',  ( 7.950000000000000178, 0.000000000000000000, 6.000000000000001776 ) ) ;
#12887=CARTESIAN_POINT ( 'NONE',  ( 62.95000000000000284, 0.000000000000000000, 5.035999999999999588 ) ) ;
#12906=SURFACE_STYLE_FILL_AREA ( #6686 ) ;
#12916=DIRECTION ( 'NONE',  ( 1.000000000000000000, 0.000000000000000000, 0.000000000000000000 ) ) ;
#12958=LINE ( 'NONE', #5106, #19451 ) ;
#12966=ORIENTED_EDGE ( 'NONE', *, *, #5903, .T. ) ;
#12977=CARTESIAN_POINT ( 'NONE',  ( -3.931715182917647021E-15, -8.014718854569428785, -4.118099735505511561 ) ) ;
#13018=CARTESIAN_POINT ( 'NONE',  ( 0.8038475772931082952, -5.196152422707021934, -8.999999999999998224 ) ) ;
#13063=DIRECTION ( 'NONE',  ( 0.000000000000000000, -0.5000000000000018874, -0.8660254037844374864 ) ) ;
#13146=VERTEX_POINT ( 'NONE', #8921 ) ;
#13184=VERTEX_POINT ( 'NONE', #5664 ) ;
#13192=CARTESIAN_POINT ( 'NONE',  ( 0.01899995639453659624, 8.236198097127171991, 3.734486434573634828 ) ) ;
#13230=ORIENTED_EDGE ( 'NONE', *, *, #3668, .F. ) ;
#13248=CARTESIAN_POINT ( 'NONE',  ( 7.350000000000000533, 10.39230484541327471, 0.000000000000000000 ) ) ;
#13265=EDGE_CURVE ( 'NONE', #2533, #17037, #300, .T. ) ;
#13331=ORIENTED_EDGE ( 'NONE', *, *, #5173, .T. ) ;
#13410=VERTEX_POINT ( 'NONE', #6451 ) ;
#13432=ORIENTED_EDGE ( 'NONE', *, *, #12258, .F. ) ;
#13445=CARTESIAN_POINT ( 'NONE',  ( 0.000000000000000000, 0.000000000000000000, 0.000000000000000000 ) ) ;
#13451=AXIS2_PLACEMENT_3D ( 'NONE', #10741, #15454, #18220 ) ;
#13454=ADVANCED_FACE ( 'NONE', ( #2438 ), #11542, .T. ) ;
#13500=DIRECTION ( 'NONE',  ( 1.000000000000000000, 0.000000000000000000, 0.000000000000000000 ) ) ;
#13502=CARTESIAN_POINT ( 'NONE',  ( 0.000000000000000000, 7.347880794884121708E-16, -6.000000000000001776 ) ) ;
#13509=ADVANCED_FACE ( 'NONE', ( #699 ), #5409, .T. ) ;
#13520=CIRCLE ( 'NONE', #14202, 9.000000000000000000 ) ;
#13521=CARTESIAN_POINT ( 'NONE',  ( 7.350000000000000533, 5.196152422706624030, -9.000000000000001776 ) ) ;
#13588=ADVANCED_FACE ( 'NONE', ( #5913 ), #5656, .T. ) ;
#13632=FACE_OUTER_BOUND ( 'NONE', #12279, .T. ) ;
#13640=EDGE_CURVE ( 'NONE', #2094, #6317, #12181, .T. ) ;
#13650=DIRECTION ( 'NONE',  ( -1.000000000000000000, -0.000000000000000000, -0.000000000000000000 ) ) ;
#13655=EDGE_CURVE ( 'NONE', #12459, #7604, #5984, .T. ) ;
#13662=DIRECTION ( 'NONE',  ( 1.000000000000000000, 0.000000000000000000, 0.000000000000000000 ) ) ;
#13680=DIRECTION ( 'NONE',  ( -0.000000000000000000, 0.000000000000000000, -1.000000000000000000 ) ) ;
#13692=B_SPLINE_CURVE_WITH_KNOTS ( 'NONE', 3,
 ( #3751, #976, #7224, #7519, #3032, #4251 ),
 .UNSPECIFIED., .F., .F.,
 ( 4, 2, 4 ),
 ( 2.380730968223946593E-07, 0.002629065763328364801, 0.005257893453559907108 ),
 .UNSPECIFIED. ) ;
#13705=CARTESIAN_POINT ( 'NONE',  ( 61.98599999999999000, 0.000000000000000000, 6.000000000000001776 ) ) ;
#13736=DIRECTION ( 'NONE',  ( -0.000000000000000000, 0.8660254037844387076, 0.4999999999999998335 ) ) ;
#13748=DIRECTION ( 'NONE',  ( 0.000000000000000000, -0.8660254037844379305, 0.5000000000000013323 ) ) ;
#13749=CARTESIAN_POINT ( 'NONE',  ( 62.95000000000000284, 0.000000000000000000, 0.000000000000000000 ) ) ;
#13771=CARTESIAN_POINT ( 'NONE',  ( 0.000000000000000000, 0.000000000000000000, 0.000000000000000000 ) ) ;
#13776=DIRECTION ( 'NONE',  ( 0.000000000000000000, 0.000000000000000000, 1.000000000000000000 ) ) ;
#13816=LINE ( 'NONE', #3089, #4168 ) ;
#13845=AXIS2_PLACEMENT_3D ( 'NONE', #702, #3872, #9913 ) ;
#13859=FACE_OUTER_BOUND ( 'NONE', #12066, .T. ) ;
#13862=CARTESIAN_POINT ( 'NONE',  ( 0.3593302862868675285, 3.504574740656562160, 9.000000000000003553 ) ) ;
#13874=ORIENTED_EDGE ( 'NONE', *, *, #15416, .T. ) ;
#13883=AXIS2_PLACEMENT_3D ( 'NONE', #19174, #9847, #12715 ) ;
#13921=DIRECTION ( 'NONE',  ( -1.000000000000000000, -0.000000000000000000, -0.000000000000000000 ) ) ;
#13954=CARTESIAN_POINT ( 'NONE',  ( 7.350000000000000533, 9.000000000000000000, 0.000000000000000000 ) ) ;
#13957=DIRECTION ( 'NONE',  ( -1.000000000000000000, -0.000000000000000000, -0.000000000000000000 ) ) ;
#13964=DIRECTION ( 'NONE',  ( 0.000000000000000000, 0.000000000000000000, -1.000000000000000000 ) ) ;
#13994=EDGE_CURVE ( 'NONE', #7604, #12459, #3403, .T. ) ;
#14064=CARTESIAN_POINT ( 'NONE',  ( 0.3563104543936055912, -6.049278984716128349, -7.522341449313002748 ) ) ;
#14117=AXIS2_PLACEMENT_3D ( 'NONE', #14359, #5059, #6590 ) ;
#14158=AXIS2_PLACEMENT_3D ( 'NONE', #3575, #2146, #17893 ) ;
#14176=CARTESIAN_POINT ( 'NONE',  ( 7.350000000000001421, 0.000000000000000000, 0.000000000000000000 ) ) ;
#14178=FACE_OUTER_BOUND ( 'NONE', #1688, .T. ) ;
#14180=CARTESIAN_POINT ( 'NONE',  ( 7.350000000000001421, 7.794228634059940042, -4.500000000000010658 ) ) ;
#14200=CARTESIAN_POINT ( 'NONE',  ( 61.98599999999999000, 7.347880794884121708E-16, -6.000000000000001776 ) ) ;
#14202=AXIS2_PLACEMENT_3D ( 'NONE', #517, #204, #8077 ) ;
#14203=DIRECTION ( 'NONE',  ( 0.000000000000000000, -0.5000000000000018874, -0.8660254037844374864 ) ) ;
#14228=LINE ( 'NONE', #6570, #15029 ) ;
#14273=CARTESIAN_POINT ( 'NONE',  ( 0.1482032042127258142, 2.204400401860216796, -9.000000000000005329 ) ) ;
#14327=LINE ( 'NONE', #9712, #11788 ) ;
#14331=CARTESIAN_POINT ( 'NONE',  ( 0.000000000000000000, 0.000000000000000000, 0.000000000000000000 ) ) ;
#14355=EDGE_CURVE ( 'NONE', #8563, #7173, #4712, .T. ) ;
#14359=CARTESIAN_POINT ( 'NONE',  ( 7.950000000000000178, 0.000000000000000000, 0.000000000000000000 ) ) ;
#14373=CARTESIAN_POINT ( 'NONE',  ( -3.892963425580764358E-15, -7.351593252548091151, -5.266666970006173898 ) ) ;
#14421=FACE_OUTER_BOUND ( 'NONE', #20016, .T. ) ;
#14440=DIRECTION ( 'NONE',  ( 0.000000000000000000, 0.000000000000000000, -1.000000000000000000 ) ) ;
#14451=CARTESIAN_POINT ( 'NONE',  ( 0.1469846612282503517, 8.891930899535431365, 2.598723904613013946 ) ) ;
#14501=EDGE_CURVE ( 'NONE', #14685, #7508, #14557, .T. ) ;
#14517=EDGE_CURVE ( 'NONE', #9431, #14685, #4379, .T. ) ;
#14518=CARTESIAN_POINT ( 'NONE',  ( 7.350000000000000533, 9.000000000000000000, 0.000000000000000000 ) ) ;
#14557=B_SPLINE_CURVE_WITH_KNOTS ( 'NONE', 3,
 ( #17827, #11575, #13192, #19713, #14451, #3705, #11924, #9641 ),
 .UNSPECIFIED., .F., .F.,
 ( 4, 2, 2, 4 ),
 ( 0.005257893453559881955, 0.006567392922673219967, 0.007876892391786557979, 0.01049589133001323747 ),
 .UNSPECIFIED. ) ;
#14597=CIRCLE ( 'NONE', #4131, 9.000000000000000000 ) ;
#14607=CARTESIAN_POINT ( 'NONE',  ( 7.350000000000000533, 9.000000000000000000, 0.000000000000000000 ) ) ;
#14685=VERTEX_POINT ( 'NONE', #8515 ) ;
#14702=FACE_OUTER_BOUND ( 'NONE', #15058, .T. ) ;
#14706=PLANE ( 'NONE',  #3397 ) ;
#14736=B_SPLINE_CURVE_WITH_KNOTS ( 'NONE', 3,
 ( #9517, #12977, #19235, #5222, #17705, #2151, #3281, #17303 ),
 .UNSPECIFIED., .F., .F.,
 ( 4, 2, 2, 4 ),
 ( 0.005257893453559887159, 0.006567392922673222569, 0.007876892391786557979, 0.01049589133001322533 ),
 .UNSPECIFIED. ) ;
#14798=LINE ( 'NONE', #8459, #6191 ) ;
#14913=ORIENTED_EDGE ( 'NONE', *, *, #17806, .T. ) ;
#14949=DIRECTION ( 'NONE',  ( 0.000000000000000000, 1.000000000000000000, -3.338476886082577323E-16 ) ) ;
#14950=ORIENTED_EDGE ( 'NONE', *, *, #4392, .T. ) ;
#14955=ADVANCED_FACE ( 'NONE', ( #9924 ), #3587, .T. ) ;
#14975=EDGE_CURVE ( 'NONE', #2533, #15182, #13520, .T. ) ;
#14989=CARTESIAN_POINT ( 'NONE',  ( 0.3563104543936318480, -9.539178283403844105, 1.477658550686873129 ) ) ;
#14992=CARTESIAN_POINT ( 'NONE',  ( 7.950000000000000178, 10.39230484541327471, 0.000000000000000000 ) ) ;
#15003=CARTESIAN_POINT ( 'NONE',  ( 0.8038475772931082952, -5.196152422707021934, -8.999999999999998224 ) ) ;
#15021=CARTESIAN_POINT ( 'NONE',  ( 0.8038475772933632024, 5.196152422706628471, 9.000000000000001776 ) ) ;
#15029=VECTOR ( 'NONE', #17516, 1000.000000000000000 ) ;
#15058=EDGE_LOOP ( 'NONE', ( #5144, #14950, #1820 ) ) ;
#15153=ORIENTED_EDGE ( 'NONE', *, *, #555, .T. ) ;
#15182=VERTEX_POINT ( 'NONE', #10816 ) ;
#15184=CARTESIAN_POINT ( 'NONE',  ( 7.950000000000000178, 5.196152422706624030, -9.000000000000001776 ) ) ;
#15208=CARTESIAN_POINT ( 'NONE',  ( 0.000000000000000000, -7.794228634059948035, -4.499999999999999112 ) ) ;
#15210=CARTESIAN_POINT ( 'NONE',  ( 0.1469846612282481035, 6.696526368584462041, -6.401276095386996268 ) ) ;
#15218=VERTEX_POINT ( 'NONE', #4590 ) ;
#15226=ORIENTED_EDGE ( 'NONE', *, *, #9980, .T. ) ;
#15286=DIRECTION ( 'NONE',  ( 0.000000000000000000, 0.000000000000000000, 1.000000000000000000 ) ) ;
#15304=DIRECTION ( 'NONE',  ( 0.000000000000000000, 0.000000000000000000, -1.000000000000000000 ) ) ;
#15305=CIRCLE ( 'NONE', #18244, 9.000000000000000000 ) ;
#15309=DIRECTION ( 'NONE',  ( 1.000000000000000000, 0.000000000000000000, 0.000000000000000000 ) ) ;
#15310=CIRCLE ( 'NONE', #8129, 9.000000000000000000 ) ;
#15342=EDGE_CURVE ( 'NONE', #7173, #7971, #12958, .T. ) ;
#15352=ORIENTED_EDGE ( 'NONE', *, *, #1534, .F. ) ;
#15361=EDGE_LOOP ( 'NONE', ( #6986, #10343, #6748, #16731 ) ) ;
#15394=DIRECTION ( 'NONE',  ( 0.000000000000000000, 0.4999999999999998335, -0.8660254037844387076 ) ) ;
#15403=CARTESIAN_POINT ( 'NONE',  ( 0.01885174614965864567, 0.8831628876357825453, 9.000000000000000000 ) ) ;
#15416=EDGE_CURVE ( 'NONE', #7173, #13146, #7032, .T. ) ;
#15454=DIRECTION ( 'NONE',  ( 0.000000000000000000, -0.8660254037844380415, -0.5000000000000009992 ) ) ;
#15475=CARTESIAN_POINT ( 'NONE',  ( 7.350000000000000533, 5.196152422706627583, 9.000000000000001776 ) ) ;
#15495=AXIS2_PLACEMENT_3D ( 'NONE', #14331, #6566, #17512 ) ;
#15501=ORIENTED_EDGE ( 'NONE', *, *, #14517, .T. ) ;
#15568=CARTESIAN_POINT ( 'NONE',  ( 0.000000000000000000, 0.000000000000000000, 0.000000000000000000 ) ) ;
#15583=CARTESIAN_POINT ( 'NONE',  ( 0.000000000000000000, 0.000000000000000000, 0.000000000000000000 ) ) ;
#15599=ORIENTED_EDGE ( 'NONE', *, *, #12660, .F. ) ;
#15607=ADVANCED_FACE ( 'NONE', ( #5354 ), #3810, .F. ) ;
#15610=CARTESIAN_POINT ( 'NONE',  ( 0.000000000000000000, -3.004629197474327134E-15, 9.000000000000000000 ) ) ;
#15627=CONICAL_SURFACE ( 'NONE', #5824, 5.035999999999999588, 0.7853981633974425058 ) ;
#15655=ADVANCED_FACE ( 'NONE', ( #448 ), #2147, .T. ) ;
#15657=ORIENTED_EDGE ( 'NONE', *, *, #964, .F. ) ;
#15676=EDGE_CURVE ( 'NONE', #6317, #18284, #2577, .T. ) ;
#15691=B_SPLINE_CURVE_WITH_KNOTS ( 'NONE', 3,
 ( #8367, #5307, #593, #7040, #19609, #15003 ),
 .UNSPECIFIED., .F., .F.,
 ( 4, 2, 4 ),
 ( 0.03045342003272952236, 0.03308352805739833702, 0.03571363608206715862 ),
 .UNSPECIFIED. ) ;
#15703=ORIENTED_EDGE ( 'NONE', *, *, #555, .F. ) ;
#15705=ORIENTED_EDGE ( 'NONE', *, *, #14355, .T. ) ;
#15732=CARTESIAN_POINT ( 'NONE',  ( 7.350000000000001421, -7.794228634059948035, -4.499999999999999112 ) ) ;
#15744=B_SPLINE_CURVE_WITH_KNOTS ( 'NONE', 3,
 ( #7949, #12552, #3353, #3258, #9592, #1514 ),
 .UNSPECIFIED., .F., .F.,
 ( 4, 2, 4 ),
 ( 2.380730968235596737E-07, 0.002629065763328352658, 0.005257893453559881955 ),
 .UNSPECIFIED. ) ;
#15774=EDGE_LOOP ( 'NONE', ( #10134, #16899 ) ) ;
#15808=FACE_OUTER_BOUND ( 'NONE', #5931, .T. ) ;
#15821=SHAPE_REPRESENTATION ( 'hex bolt gradec_iso_ISO 4016 - M12 x 55 x 30-WN', ( #18639 ), #2627 ) ;
#15860=VERTEX_POINT ( 'NONE', #17517 ) ;
#15864=PRODUCT_DEFINITION_SHAPE ( 'NONE', 'NONE',  #8394 ) ;
#15871=APPLICATION_CONTEXT ( 'automotive_design' ) ;
#15877=DIRECTION ( 'NONE',  ( -1.000000000000000000, -0.000000000000000000, 0.000000000000000000 ) ) ;
#15954=CARTESIAN_POINT ( 'NONE',  ( 7.350000000000000533, 5.196152422706624030, -9.000000000000001776 ) ) ;
#15983=EDGE_LOOP ( 'NONE', ( #19325, #4986, #8835 ) ) ;
#15984=AXIS2_PLACEMENT_3D ( 'NONE', #8945, #5585, #5690 ) ;
#16034=ORIENTED_EDGE ( 'NONE', *, *, #2402, .T. ) ;
#16075=CARTESIAN_POINT ( 'NONE',  ( 7.350000000000000533, -5.196152422706636465, -8.999999999999998224 ) ) ;
#16082=ORIENTED_EDGE ( 'NONE', *, *, #19496, .F. ) ;
#16123=VERTEX_POINT ( 'NONE', #2857 ) ;
#16126=ORIENTED_EDGE ( 'NONE', *, *, #5153, .F. ) ;
#16214=CARTESIAN_POINT ( 'NONE',  ( 0.01885174614965866302, 0.8831628876357845437, -9.000000000000001776 ) ) ;
#16215=B_SPLINE_CURVE_WITH_KNOTS ( 'NONE', 3,
 ( #2204, #9862, #11496, #14273, #19289, #16214, #9966, #19188 ),
 .UNSPECIFIED., .F., .F.,
 ( 4, 2, 2, 4 ),
 ( 0.02518894967656377937, 0.02782118485464665086, 0.02913730244368808661, 0.03045342003272952236 ),
 .UNSPECIFIED. ) ;
#16433=AXIS2_PLACEMENT_3D ( 'NONE', #8086, #15877, #14440 ) ;
#16440=AXIS2_PLACEMENT_3D ( 'NONE', #13771, #15309, #4467 ) ;
#16463=VECTOR ( 'NONE', #19513, 1000.000000000000000 ) ;
#16502=CARTESIAN_POINT ( 'NONE',  ( 7.350000000000000533, 5.196152422706624030, -9.000000000000001776 ) ) ;
#16550=EDGE_LOOP ( 'NONE', ( #16126, #14913, #9979, #281, #3570, #12635 ) ) ;
#16552=CARTESIAN_POINT ( 'NONE',  ( 7.950000000000000178, -5.196152422706636465, -8.999999999999998224 ) ) ;
#16555=DIRECTION ( 'NONE',  ( -1.000000000000000000, -0.000000000000000000, -0.000000000000000000 ) ) ;
#16593=EDGE_LOOP ( 'NONE', ( #16676, #4257, #18709, #3925, #1863, #5668 ) ) ;
#16613=EDGE_CURVE ( 'NONE', #166, #9431, #3235, .T. ) ;
#16635=CARTESIAN_POINT ( 'NONE',  ( 0.000000000000000000, -7.794228634059936489, 4.500000000000017764 ) ) ;
#16676=ORIENTED_EDGE ( 'NONE', *, *, #17739, .F. ) ;
#16678=VERTEX_POINT ( 'NONE', #16075 ) ;
#16721=ORIENTED_EDGE ( 'NONE', *, *, #3510, .T. ) ;
#16731=ORIENTED_EDGE ( 'NONE', *, *, #1999, .F. ) ;
#16826=DIRECTION ( 'NONE',  ( -1.000000000000000000, -0.000000000000000000, -0.000000000000000000 ) ) ;
#16854=ORIENTED_EDGE ( 'NONE', *, *, #19904, .F. ) ;
#16871=ORIENTED_EDGE ( 'NONE', *, *, #8246, .F. ) ;
#16872=AXIS2_PLACEMENT_3D ( 'NONE', #10603, #9184, #13680 ) ;
#16880=CARTESIAN_POINT ( 'NONE',  ( 7.950000000000000178, 5.196152422706624030, -9.000000000000001776 ) ) ;
#16899=ORIENTED_EDGE ( 'NONE', *, *, #7085, .T. ) ;
#16907=VECTOR ( 'NONE', #11708, 1000.000000000000000 ) ;
#16958=CARTESIAN_POINT ( 'NONE',  ( 0.1469846612282419140, -6.696526368584444278, 6.401276095387000709 ) ) ;
#16962=CARTESIAN_POINT ( 'NONE',  ( 0.09252763182291959265, 6.914127053141843504, -6.024380653971843635 ) ) ;
#16972=CARTESIAN_POINT ( 'NONE',  ( 7.350000000000000533, -5.196152422706636465, -8.999999999999998224 ) ) ;
#17037=VERTEX_POINT ( 'NONE', #17074 ) ;
#17048=DIRECTION ( 'NONE',  ( 1.000000000000000000, 0.000000000000000000, 0.000000000000000000 ) ) ;
#17063=CARTESIAN_POINT ( 'NONE',  ( 0.000000000000000000, -7.794228634059936489, 4.500000000000017764 ) ) ;
#17074=CARTESIAN_POINT ( 'NONE',  ( 7.350000000000000533, 10.39230484541327471, 0.000000000000000000 ) ) ;
#17088=EDGE_LOOP ( 'NONE', ( #4165, #875, #12011, #17323, #15501, #3834 ) ) ;
#17100=FACE_OUTER_BOUND ( 'NONE', #15983, .T. ) ;
#17102=VECTOR ( 'NONE', #13063, 1000.000000000000114 ) ;
#17115=CARTESIAN_POINT ( 'NONE',  ( 7.350000000000000533, -10.39230484541326582, 0.000000000000000000 ) ) ;
#17135=ORIENTED_EDGE ( 'NONE', *, *, #13640, .F. ) ;
#17303=CARTESIAN_POINT ( 'NONE',  ( 0.8038475772933646457, -10.39230484541326582, 2.804506490479260738E-17 ) ) ;
#17323=ORIENTED_EDGE ( 'NONE', *, *, #2402, .F. ) ;
#17392=EDGE_CURVE ( 'NONE', #17037, #19269, #8462, .T. ) ;
#17405=DIRECTION ( 'NONE',  ( 0.000000000000000000, -1.000000000000000000, -3.338476886082585705E-16 ) ) ;
#17413=ADVANCED_FACE ( 'NONE', ( #14702 ), #8361, .T. ) ;
#17435=SURFACE_STYLE_USAGE ( .BOTH. , #3798 ) ;
#17458=DIRECTION ( 'NONE',  ( -1.000000000000000000, -0.000000000000000000, -0.000000000000000000 ) ) ;
#17512=DIRECTION ( 'NONE',  ( 0.000000000000000000, 0.000000000000000000, 1.000000000000000000 ) ) ;
#17516=DIRECTION ( 'NONE',  ( -1.000000000000000000, -0.000000000000000000, -0.000000000000000000 ) ) ;
#17517=CARTESIAN_POINT ( 'NONE',  ( 0.8038475772933632024, 5.196152422706628471, 9.000000000000001776 ) ) ;
#17527=ADVANCED_BREP_SHAPE_REPRESENTATION ( '', ( #8063, #18639 ), #2627 ) ;
#17534=( NAMED_UNIT ( * ) SI_UNIT ( $, .STERADIAN. ) SOLID_ANGLE_UNIT ( ) );
#17564=DIRECTION ( 'NONE',  ( 0.000000000000000000, 0.8660254037844375974, -0.5000000000000019984 ) ) ;
#17629=CONICAL_SURFACE ( 'NONE', #15984, 9.000000000000000000, 1.047197551196600296 ) ;
#17663=PLANE ( 'NONE',  #682 ) ;
#17691=EDGE_CURVE ( 'NONE', #16123, #15218, #17914, .T. ) ;
#17693=FACE_BOUND ( 'NONE', #15774, .T. ) ;
#17705=CARTESIAN_POINT ( 'NONE',  ( 0.1469846612282495468, -8.891930899535427812, -2.598723904613008617 ) ) ;
#17739=EDGE_CURVE ( 'NONE', #12589, #2533, #18226, .T. ) ;
#17806=EDGE_CURVE ( 'NONE', #5943, #166, #13816, .T. ) ;
#17827=CARTESIAN_POINT ( 'NONE',  ( 0.000000000000000000, 7.794228634059941818, 4.500000000000007994 ) ) ;
#17863=ADVANCED_FACE ( 'NONE', ( #17100 ), #11698, .T. ) ;
#17864=EDGE_LOOP ( 'NONE', ( #8938, #7655, #15705 ) ) ;
#17880=DIRECTION ( 'NONE',  ( -1.000000000000000000, -0.000000000000000000, -0.000000000000000000 ) ) ;
#17888=CARTESIAN_POINT ( 'NONE',  ( 7.350000000000000533, 9.000000000000000000, 0.000000000000000000 ) ) ;
#17893=DIRECTION ( 'NONE',  ( 0.000000000000000000, 0.000000000000000000, -1.000000000000000000 ) ) ;
#17914=CIRCLE ( 'NONE', #11035, 9.000000000000000000 ) ;
#18031=DIRECTION ( 'NONE',  ( 0.000000000000000000, 0.000000000000000000, 1.000000000000000000 ) ) ;
#18068=AXIS2_PLACEMENT_3D ( 'NONE', #5602, #11819, #18085 ) ;
#18077=COLOUR_RGB ( '', 0.72549020, 0.75294118, 0.79215686) ;
#18085=DIRECTION ( 'NONE',  ( 0.000000000000000000, 0.000000000000000000, 1.000000000000000000 ) ) ;
#18104=ORIENTED_EDGE ( 'NONE', *, *, #1990, .T. ) ;
#18164=CARTESIAN_POINT ( 'NONE',  ( 0.07661102881317166657, -8.673996836102537245, 2.976196775178697962 ) ) ;
#18193=DIRECTION ( 'NONE',  ( 0.000000000000000000, 0.000000000000000000, -1.000000000000000000 ) ) ;
#18198=LINE ( 'NONE', #16972, #670 ) ;
#18220=DIRECTION ( 'NONE',  ( 0.000000000000000000, 0.5000000000000009992, -0.8660254037844380415 ) ) ;
#18226=LINE ( 'NONE', #16502, #3206 ) ;
#18244=AXIS2_PLACEMENT_3D ( 'NONE', #4791, #6225, #13776 ) ;
#18264=DIRECTION ( 'NONE',  ( 0.000000000000000000, 0.000000000000000000, 1.000000000000000000 ) ) ;
#18284=VERTEX_POINT ( 'NONE', #11909 ) ;
#18314=ORIENTED_EDGE ( 'NONE', *, *, #9980, .F. ) ;
#18327=CARTESIAN_POINT ( 'NONE',  ( 0.5595136366802131445, -4.349754824395698272, 9.000000000000000000 ) ) ;
#18329=DIRECTION ( 'NONE',  ( -1.000000000000000000, -0.000000000000000000, -0.000000000000000000 ) ) ;
#18363=EDGE_CURVE ( 'NONE', #17037, #7508, #19411, .T. ) ;
#18386=ORIENTED_EDGE ( 'NONE', *, *, #14501, .T. ) ;
#18397=CARTESIAN_POINT ( 'NONE',  ( 0.8038475772933615371, 5.196152422706624030, -9.000000000000001776 ) ) ;
#18473=CARTESIAN_POINT ( 'NONE',  ( 0.09318607064769283965, 1.767053008364804834, 8.999999999999998224 ) ) ;
#18480=ADVANCED_FACE ( 'NONE', ( #13859 ), #4451, .T. ) ;
#18532=EDGE_CURVE ( 'NONE', #12459, #6317, #1796, .T. ) ;
#18565=VECTOR ( 'NONE', #5208, 1000.000000000000000 ) ;
#18588=EDGE_CURVE ( 'NONE', #15182, #8563, #15310, .T. ) ;
#18620=APPLICATION_CONTEXT ( 'automotive_design' ) ;
#18639=AXIS2_PLACEMENT_3D ( 'NONE', #8416, #18031, #13500 ) ;
#18661=ADVANCED_FACE ( 'NONE', ( #1046 ), #7002, .T. ) ;
#18679=ORIENTED_EDGE ( 'NONE', *, *, #1990, .F. ) ;
#18709=ORIENTED_EDGE ( 'NONE', *, *, #8475, .F. ) ;
#18768=DIRECTION ( 'NONE',  ( 0.000000000000000000, -1.000000000000000000, -3.338476886082585705E-16 ) ) ;
#18804=PRODUCT ( 'hex bolt gradec_iso_ISO 4016 - M12 x 55 x 30-WN', 'hex bolt gradec_iso_ISO 4016 - M12 x 55 x 30-WN', '', ( #20170 ) ) ;
#18806=CARTESIAN_POINT ( 'NONE',  ( 0.000000000000000000, 0.000000000000000000, 0.000000000000000000 ) ) ;
#18957=ORIENTED_EDGE ( 'NONE', *, *, #13265, .T. ) ;
#18962=EDGE_LOOP ( 'NONE', ( #16854, #16721, #16082, #5699, #5972, #18679 ) ) ;
#18992=DIRECTION ( 'NONE',  ( -1.000000000000000000, -0.000000000000000000, -0.000000000000000000 ) ) ;
#19011=CARTESIAN_POINT ( 'NONE',  ( 0.8038475772933556529, -5.196152422706607155, 8.999999999999998224 ) ) ;
#19069=AXIS2_PLACEMENT_3D ( 'NONE', #14518, #10111, #19516 ) ;
#19086=PLANE ( 'NONE',  #1102 ) ;
#19159=PRESENTATION_STYLE_ASSIGNMENT (( #17435 ) ) ;
#19174=CARTESIAN_POINT ( 'NONE',  ( 7.950000000000000178, 5.196152422706627583, 9.000000000000001776 ) ) ;
#19188=CARTESIAN_POINT ( 'NONE',  ( 0.000000000000000000, -3.004629197474319246E-15, -9.000000000000000000 ) ) ;
#19214=ORIENTED_EDGE ( 'NONE', *, *, #11972, .F. ) ;
#19235=CARTESIAN_POINT ( 'NONE',  ( 0.01899995639453602378, -8.236198097127177320, -3.734486434573622393 ) ) ;
#19269=VERTEX_POINT ( 'NONE', #11251 ) ;
#19289=CARTESIAN_POINT ( 'NONE',  ( 0.09318607064769274251, 1.767053008364804834, -9.000000000000001776 ) ) ;
#19325=ORIENTED_EDGE ( 'NONE', *, *, #5638, .T. ) ;
#19330=DIRECTION ( 'NONE',  ( 0.000000000000000000, 0.000000000000000000, -1.000000000000000000 ) ) ;
#19406=LINE ( 'NONE', #869, #16907 ) ;
#19411=LINE ( 'NONE', #14992, #12373 ) ;
#19426=AXIS2_PLACEMENT_3D ( 'NONE', #2921, #7512, #10784 ) ;
#19431=CARTESIAN_POINT ( 'NONE',  ( 7.350000000000000533, 9.000000000000000000, 0.000000000000000000 ) ) ;
#19451=VECTOR ( 'NONE', #14203, 1000.000000000000114 ) ;
#19496=EDGE_CURVE ( 'NONE', #9431, #15860, #8501, .T. ) ;
#19502=FACE_OUTER_BOUND ( 'NONE', #1657, .T. ) ;
#19513=DIRECTION ( 'NONE',  ( -1.000000000000000000, -0.000000000000000000, -0.000000000000000000 ) ) ;
#19516=DIRECTION ( 'NONE',  ( 0.000000000000000000, 0.000000000000000000, -1.000000000000000000 ) ) ;
#19576=CARTESIAN_POINT ( 'NONE',  ( 0.000000000000000000, 0.000000000000000000, 0.000000000000000000 ) ) ;
#19592=ORIENTED_EDGE ( 'NONE', *, *, #19904, .T. ) ;
#19609=CARTESIAN_POINT ( 'NONE',  ( 0.5595136366802733185, -4.349754824395939856, -8.999999999999998224 ) ) ;
#19626=CIRCLE ( 'NONE', #5275, 9.000000000000000000 ) ;
#19645=ORIENTED_EDGE ( 'NONE', *, *, #13655, .T. ) ;
#19646=PLANE ( 'NONE',  #8343 ) ;
#19659=ADVANCED_FACE ( 'NONE', ( #11199 ), #17663, .F. ) ;
#19713=CARTESIAN_POINT ( 'NONE',  ( 0.09252763182292092492, 8.674330214978045461, 2.975619346028168355 ) ) ;
#19838=DIRECTION ( 'NONE',  ( -1.000000000000000000, -0.000000000000000000, -0.000000000000000000 ) ) ;
#19850=CARTESIAN_POINT ( 'NONE',  ( -3.049318610115479988E-17, -0.8794428697894424163, 9.000000000000000000 ) ) ;
#19894=DIRECTION ( 'NONE',  ( 0.000000000000000000, -0.5000000000000013323, -0.8660254037844380415 ) ) ;
#19904=EDGE_CURVE ( 'NONE', #13184, #13146, #5877, .T. ) ;
#19961=( LENGTH_UNIT ( ) NAMED_UNIT ( * ) SI_UNIT ( .MILLI., .METRE. ) );
#19980=DIRECTION ( 'NONE',  ( 0.000000000000000000, -0.4999999999999998335, 0.8660254037844387076 ) ) ;
#20016=EDGE_LOOP ( 'NONE', ( #18957, #12328, #8620 ) ) ;
#20101=EDGE_LOOP ( 'NONE', ( #15703, #8350, #8153, #6351, #19214, #5309 ) ) ;
#20102=DIRECTION ( 'NONE',  ( -1.000000000000000000, -0.000000000000000000, -0.000000000000000000 ) ) ;
#20160=CARTESIAN_POINT ( 'NONE',  ( 0.07568653364411945250, -1.751902528157375905, 8.999999999999996447 ) ) ;
#20170=PRODUCT_CONTEXT ( 'NONE', #15871, 'mechanical' ) ;
#20193=AXIS2_PLACEMENT_3D ( 'NONE', #15568, #7783, #6062 ) ;
#20197=DIRECTION ( 'NONE',  ( 1.000000000000000000, 0.000000000000000000, 0.000000000000000000 ) ) ;
#20200=DIRECTION ( 'NONE',  ( 0.000000000000000000, 0.000000000000000000, 1.000000000000000000 ) ) ;
#20237=CONICAL_SURFACE ( 'NONE', #6544, 5.035999999999999588, 0.7853981633974425058 ) ;
ENDSEC;
END-ISO-10303-21;
